ISO-10303-21;
HEADER;
/* Generated by software containing ST-Developer
 * from STEP Tools, Inc. (www.steptools.com) 
 */

FILE_DESCRIPTION(
/* description */ ('PAT-091'),
/* implementation_level */ '2;1');

FILE_NAME(
/* name */ 'M4 low-profile retaining screw (10).step',
/* time_stamp */ '2026-10-27T15:34:44-07:00',
/* author */ (''),
/* organization */ (''),
/* preprocessor_version */ 'ST-DEVELOPER v20.2',
/* originating_system */ 'Autodesk Translation Framework v15.17.0.0',
/* authorisation */ '');

FILE_SCHEMA (('AUTOMOTIVE_DESIGN { 1 0 10303 214 3 1 1 }'));
ENDSEC;

DATA;
#10=MECHANICAL_DESIGN_GEOMETRIC_PRESENTATION_REPRESENTATION('',(#1063),#25100);
#843=SHAPE_REPRESENTATION_RELATIONSHIP('SRR','None',#25610,#953);
#953=ADVANCED_BREP_SHAPE_REPRESENTATION('',(#1184),#25080);
#1063=STYLED_ITEM('',(#26198),#1184);
#1184=MANIFOLD_SOLID_BREP('Body1',#13343);
#1601=FACE_BOUND('',#3942,.T.);
#2004=PLANE('',#16052);
#2005=PLANE('',#16057);
#2006=PLANE('',#16060);
#2737=FACE_OUTER_BOUND('',#3941,.T.);
#2738=FACE_OUTER_BOUND('',#3943,.T.);
#2739=FACE_OUTER_BOUND('',#3944,.T.);
#2740=FACE_OUTER_BOUND('',#3945,.T.);
#2741=FACE_OUTER_BOUND('',#3946,.T.);
#3941=EDGE_LOOP('',(#11600));
#3942=EDGE_LOOP('',(#11601));
#3943=EDGE_LOOP('',(#11602,#11603,#11604,#11605));
#3944=EDGE_LOOP('',(#11606));
#3945=EDGE_LOOP('',(#11607,#11608,#11609,#11610));
#3946=EDGE_LOOP('',(#11611));
#4816=LINE('',#24068,#5556);
#4817=LINE('',#24074,#5557);
#5556=VECTOR('',#20102,0.350000000000001);
#5557=VECTOR('',#20111,0.199999999999999);
#6222=CIRCLE('',#16053,0.350000000000001);
#6223=CIRCLE('',#16054,0.199999999999999);
#6224=CIRCLE('',#16056,0.350000000000001);
#6225=CIRCLE('',#16059,0.199999999999999);
#7255=VERTEX_POINT('',#24062);
#7256=VERTEX_POINT('',#24064);
#7257=VERTEX_POINT('',#24067);
#7258=VERTEX_POINT('',#24072);
#8735=EDGE_CURVE('',#7255,#7255,#6222,.T.);
#8736=EDGE_CURVE('',#7256,#7256,#6223,.T.);
#8737=EDGE_CURVE('',#7255,#7257,#4816,.T.);
#8738=EDGE_CURVE('',#7257,#7257,#6224,.T.);
#8739=EDGE_CURVE('',#7258,#7258,#6225,.T.);
#8740=EDGE_CURVE('',#7258,#7256,#4817,.T.);
#11600=ORIENTED_EDGE('',*,*,#8735,.T.);
#11601=ORIENTED_EDGE('',*,*,#8736,.F.);
#11602=ORIENTED_EDGE('',*,*,#8735,.F.);
#11603=ORIENTED_EDGE('',*,*,#8737,.T.);
#11604=ORIENTED_EDGE('',*,*,#8738,.T.);
#11605=ORIENTED_EDGE('',*,*,#8737,.F.);
#11606=ORIENTED_EDGE('',*,*,#8738,.F.);
#11607=ORIENTED_EDGE('',*,*,#8739,.F.);
#11608=ORIENTED_EDGE('',*,*,#8740,.T.);
#11609=ORIENTED_EDGE('',*,*,#8736,.T.);
#11610=ORIENTED_EDGE('',*,*,#8740,.F.);
#11611=ORIENTED_EDGE('',*,*,#8739,.T.);
#12372=CYLINDRICAL_SURFACE('',#16055,0.350000000000001);
#12373=CYLINDRICAL_SURFACE('',#16058,0.199999999999999);
#13104=ADVANCED_FACE('',(#2737,#1601),#2004,.T.);
#13105=ADVANCED_FACE('',(#2738),#12372,.T.);
#13106=ADVANCED_FACE('',(#2739),#2005,.F.);
#13107=ADVANCED_FACE('',(#2740),#12373,.T.);
#13108=ADVANCED_FACE('',(#2741),#2006,.T.);
#13343=CLOSED_SHELL('',(#13104,#13105,#13106,#13107,#13108));
#16051=AXIS2_PLACEMENT_3D('',#24060,#20092,#20093);
#16052=AXIS2_PLACEMENT_3D('',#24061,#20094,#20095);
#16053=AXIS2_PLACEMENT_3D('',#24063,#20096,#20097);
#16054=AXIS2_PLACEMENT_3D('',#24065,#20098,#20099);
#16055=AXIS2_PLACEMENT_3D('',#24066,#20100,#20101);
#16056=AXIS2_PLACEMENT_3D('',#24069,#20103,#20104);
#16057=AXIS2_PLACEMENT_3D('',#24070,#20105,#20106);
#16058=AXIS2_PLACEMENT_3D('',#24071,#20107,#20108);
#16059=AXIS2_PLACEMENT_3D('',#24073,#20109,#20110);
#16060=AXIS2_PLACEMENT_3D('',#24075,#20112,#20113);
#20092=DIRECTION('axis',(0.,0.,1.));
#20093=DIRECTION('refdir',(1.,0.,0.));
#20094=DIRECTION('center_axis',(0.,1.,0.));
#20095=DIRECTION('ref_axis',(1.,0.,0.));
#20096=DIRECTION('center_axis',(0.,1.,0.));
#20097=DIRECTION('ref_axis',(1.,0.,0.));
#20098=DIRECTION('center_axis',(0.,1.,0.));
#20099=DIRECTION('ref_axis',(1.,0.,0.));
#20100=DIRECTION('center_axis',(0.,1.,0.));
#20101=DIRECTION('ref_axis',(1.,0.,0.));
#20102=DIRECTION('',(0.,-1.,0.));
#20103=DIRECTION('center_axis',(0.,1.,0.));
#20104=DIRECTION('ref_axis',(1.,0.,0.));
#20105=DIRECTION('center_axis',(0.,1.,0.));
#20106=DIRECTION('ref_axis',(1.,0.,0.));
#20107=DIRECTION('center_axis',(0.,1.,0.));
#20108=DIRECTION('ref_axis',(1.,0.,0.));
#20109=DIRECTION('center_axis',(0.,1.,0.));
#20110=DIRECTION('ref_axis',(1.,0.,0.));
#20111=DIRECTION('',(0.,-1.,0.));
#20112=DIRECTION('center_axis',(0.,1.,0.));
#20113=DIRECTION('ref_axis',(1.,0.,0.));
#24060=CARTESIAN_POINT('',(0.,0.,0.));
#24061=CARTESIAN_POINT('Origin',(18.056769185842,6.7,6.69185245480489));
#24062=CARTESIAN_POINT('',(17.706769185842,6.7,6.69185245480489));
#24063=CARTESIAN_POINT('Origin',(18.056769185842,6.7,6.69185245480489));
#24064=CARTESIAN_POINT('',(17.856769185842,6.7,6.69185245480489));
#24065=CARTESIAN_POINT('Origin',(18.056769185842,6.7,6.69185245480489));
#24066=CARTESIAN_POINT('Origin',(18.056769185842,6.6,6.69185245480489));
#24067=CARTESIAN_POINT('',(17.706769185842,6.6,6.69185245480489));
#24068=CARTESIAN_POINT('',(17.706769185842,6.6,6.69185245480489));
#24069=CARTESIAN_POINT('Origin',(18.056769185842,6.6,6.69185245480489));
#24070=CARTESIAN_POINT('Origin',(18.056769185842,6.6,6.69185245480489));
#24071=CARTESIAN_POINT('Origin',(18.056769185842,6.7,6.69185245480489));
#24072=CARTESIAN_POINT('',(17.856769185842,7.4,6.69185245480489));
#24073=CARTESIAN_POINT('Origin',(18.056769185842,7.4,6.69185245480489));
#24074=CARTESIAN_POINT('',(17.856769185842,6.7,6.69185245480489));
#24075=CARTESIAN_POINT('Origin',(18.056769185842,7.4,6.69185245480489));
#24959=UNCERTAINTY_MEASURE_WITH_UNIT(LENGTH_MEASURE(0.001),#25101,
'DISTANCE_ACCURACY_VALUE',
'Maximum model space distance between geometric entities at asserted c
onnectivities');
#24979=UNCERTAINTY_MEASURE_WITH_UNIT(LENGTH_MEASURE(0.001),#25101,
'DISTANCE_ACCURACY_VALUE',
'Maximum model space distance between geometric entities at asserted c
onnectivities');
#25080=(
GEOMETRIC_REPRESENTATION_CONTEXT(3)
GLOBAL_UNCERTAINTY_ASSIGNED_CONTEXT((#24959))
GLOBAL_UNIT_ASSIGNED_CONTEXT((#25101,#25103,#25104))
REPRESENTATION_CONTEXT('','3D')
);
#25100=(
GEOMETRIC_REPRESENTATION_CONTEXT(3)
GLOBAL_UNCERTAINTY_ASSIGNED_CONTEXT((#24979))
GLOBAL_UNIT_ASSIGNED_CONTEXT((#25101,#25103,#25104))
REPRESENTATION_CONTEXT('','3D')
);
#25101=(
LENGTH_UNIT()
NAMED_UNIT(*)
SI_UNIT(.CENTI.,.METRE.)
);
#25103=(
NAMED_UNIT(*)
PLANE_ANGLE_UNIT()
SI_UNIT($,.RADIAN.)
);
#25104=(
NAMED_UNIT(*)
SI_UNIT($,.STERADIAN.)
SOLID_ANGLE_UNIT()
);
#25205=SHAPE_DEFINITION_REPRESENTATION(#25399,#25610);
#25399=PRODUCT_DEFINITION_SHAPE('',$,#25731);
#25610=SHAPE_REPRESENTATION('',(#16051),#25080);
#25630=PRODUCT_DEFINITION_CONTEXT('part definition',#25992,'design');
#25731=PRODUCT_DEFINITION('M4 low-profile retaining screw (10)',
'M4 low-profile retaining screw (10)',#25851,#25630);
#25851=PRODUCT_DEFINITION_FORMATION('',$,#26094);
#25992=APPLICATION_CONTEXT(
'Core Data for Automotive Mechanical Design Process');
#25993=PRODUCT_CONTEXT('part definition',#25992,'mechanical');
#26094=PRODUCT('M4 low-profile retaining screw (10)',
'M4 low-profile retaining screw (10)','M4 low-profile retaining screw (10)',
(#25993));
#26192=COLOUR_RGB('Black',0.12,0.14,0.17);
#26193=FILL_AREA_STYLE_COLOUR('',#26192);
#26194=FILL_AREA_STYLE('',(#26193));
#26195=SURFACE_STYLE_FILL_AREA(#26194);
#26196=SURFACE_SIDE_STYLE('',(#26195));
#26197=SURFACE_STYLE_USAGE(.BOTH.,#26196);
#26198=PRESENTATION_STYLE_ASSIGNMENT((#26197));
ENDSEC;
END-ISO-10303-21;
